ISO-10303-21;
HEADER;
FILE_DESCRIPTION (('STEP AP214'),
    '1' );
FILE_NAME ('Connector.step',
    '2026-10-28T16:39:03',
    ( '' ),
    ( '' ),
    'SwSTEP 2.0',
    'SolidWorks 2024',
    '' );
FILE_SCHEMA (( 'AUTOMOTIVE_DESIGN' ));
ENDSEC;

DATA;
#8=CARTESIAN_POINT ( 'NONE',  ( 3.081487911019577803E-31, -25.00000000000000355, 37.50000000000000000 ) ) ;
#21=DIRECTION ( 'NONE',  ( 0.000000000000000000, 0.000000000000000000, -1.000000000000000000 ) ) ;
#32=DIRECTION ( 'NONE',  ( 1.000000000000000000, 0.000000000000000000, 0.000000000000000000 ) ) ;
#36=VERTEX_POINT ( 'NONE', #5235 ) ;
#42=CIRCLE ( 'NONE', #1071, 15.64999999999999680 ) ;
#80=LINE ( 'NONE', #2529, #4060 ) ;
#107=VERTEX_POINT ( 'NONE', #1630 ) ;
#114=AXIS2_PLACEMENT_3D ( 'NONE', #4743, #7238, #7119 ) ;
#126=EDGE_CURVE ( 'NONE', #36, #6483, #6084, .T. ) ;
#138=ORIENTED_EDGE ( 'NONE', *, *, #4119, .T. ) ;
#147=EDGE_CURVE ( 'NONE', #3810, #7620, #42, .T. ) ;
#157=ORIENTED_EDGE ( 'NONE', *, *, #2928, .F. ) ;
#182=AXIS2_PLACEMENT_3D ( 'NONE', #3889, #3931, #5783 ) ;
#188=DIRECTION ( 'NONE',  ( -0.000000000000000000, 1.000000000000000000, 1.387778780781445676E-16 ) ) ;
#191=AXIS2_PLACEMENT_3D ( 'NONE', #4745, #5352, #4181 ) ;
#205=PRODUCT_DEFINITION_SHAPE ( 'NONE', 'NONE',  #7468 ) ;
#221=VERTEX_POINT ( 'NONE', #3041 ) ;
#225=ADVANCED_FACE ( 'NONE', ( #476, #7811 ), #2320, .T. ) ;
#236=EDGE_CURVE ( 'NONE', #6254, #1115, #1341, .T. ) ;
#247=ORIENTED_EDGE ( 'NONE', *, *, #2358, .F. ) ;
#250=ORIENTED_EDGE ( 'NONE', *, *, #6570, .T. ) ;
#256=DIRECTION ( 'NONE',  ( 0.000000000000000000, 0.000000000000000000, -1.000000000000000000 ) ) ;
#272=DIRECTION ( 'NONE',  ( 1.000000000000000000, -1.232595164407830946E-32, -1.710569414459005214E-48 ) ) ;
#277=ORIENTED_EDGE ( 'NONE', *, *, #1080, .F. ) ;
#304=DIRECTION ( 'NONE',  ( 1.000000000000000000, 0.000000000000000000, 0.000000000000000000 ) ) ;
#314=CYLINDRICAL_SURFACE ( 'NONE', #6244, 12.50000000000000000 ) ;
#320=PLANE ( 'NONE',  #7361 ) ;
#323=EDGE_CURVE ( 'NONE', #1563, #1167, #4526, .T. ) ;
#327=FACE_OUTER_BOUND ( 'NONE', #5998, .T. ) ;
#375=ADVANCED_FACE ( 'NONE', ( #7042 ), #7595, .T. ) ;
#376=DIRECTION ( 'NONE',  ( 0.000000000000000000, 0.000000000000000000, -1.000000000000000000 ) ) ;
#401=EDGE_LOOP ( 'NONE', ( #6678, #4952, #1055, #6847 ) ) ;
#407=ORIENTED_EDGE ( 'NONE', *, *, #6151, .F. ) ;
#408=ORIENTED_EDGE ( 'NONE', *, *, #2734, .F. ) ;
#410=CIRCLE ( 'NONE', #3617, 11.64999999999996660 ) ;
#423=FACE_OUTER_BOUND ( 'NONE', #6935, .T. ) ;
#430=SHAPE_REPRESENTATION_RELATIONSHIP ( 'NONE' , 'NONE' ,  #2073, #3260 ) ;
#435=DIRECTION ( 'NONE',  ( 0.000000000000000000, 0.000000000000000000, -1.000000000000000000 ) ) ;
#459=CARTESIAN_POINT ( 'NONE',  ( 15.64999999999999680, 1.916572240665607593E-15, 195.9999999999999716 ) ) ;
#476=FACE_OUTER_BOUND ( 'NONE', #5695, .T. ) ;
#499=CARTESIAN_POINT ( 'NONE',  ( 0.000000000000000000, 0.000000000000000000, 200.0000000000000000 ) ) ;
#509=CARTESIAN_POINT ( 'NONE',  ( -25.00000000000000000, 25.00000000000000000, 0.000000000000000000 ) ) ;
#526=CARTESIAN_POINT ( 'NONE',  ( -25.00000000000000000, 0.000000000000000000, 0.000000000000000000 ) ) ;
#533=DIRECTION ( 'NONE',  ( 0.000000000000000000, -1.481552359947913884E-16, 1.000000000000000000 ) ) ;
#544=PLANE ( 'NONE',  #945 ) ;
#550=ORIENTED_EDGE ( 'NONE', *, *, #4306, .F. ) ;
#554=ADVANCED_FACE ( 'NONE', ( #1738 ), #3476, .T. ) ;
#564=VECTOR ( 'NONE', #4224, 1000.000000000000000 ) ;
#569=ADVANCED_FACE ( 'NONE', ( #2956, #423 ), #1665, .T. ) ;
#582=CARTESIAN_POINT ( 'NONE',  ( -11.64999999999996660, 0.000000000000000000, 200.0000000000000000 ) ) ;
#586=VECTOR ( 'NONE', #272, 1000.000000000000000 ) ;
#595=CYLINDRICAL_SURFACE ( 'NONE', #3402, 15.64999999999999680 ) ;
#598=ADVANCED_FACE ( 'NONE', ( #4659 ), #544, .T. ) ;
#619=CARTESIAN_POINT ( 'NONE',  ( -25.00000000000000000, -25.00000000000000000, 0.000000000000000000 ) ) ;
#646=VERTEX_POINT ( 'NONE', #7437 ) ;
#656=FACE_OUTER_BOUND ( 'NONE', #7185, .T. ) ;
#664=DIRECTION ( 'NONE',  ( -0.000000000000000000, 0.000000000000000000, 1.000000000000000000 ) ) ;
#695=VECTOR ( 'NONE', #7305, 1000.000000000000000 ) ;
#717=EDGE_CURVE ( 'NONE', #1167, #7818, #2890, .T. ) ;
#762=CARTESIAN_POINT ( 'NONE',  ( -12.50000000000000000, 25.00000000000000000, 0.000000000000000000 ) ) ;
#790=CARTESIAN_POINT ( 'NONE',  ( 0.000000000000000000, 0.000000000000000000, 195.9999999999999716 ) ) ;
#808=DIRECTION ( 'NONE',  ( 0.000000000000000000, 0.000000000000000000, -1.000000000000000000 ) ) ;
#816=DIRECTION ( 'NONE',  ( -1.000000000000000000, -0.000000000000000000, -0.000000000000000000 ) ) ;
#823=ORIENTED_EDGE ( 'NONE', *, *, #5572, .F. ) ;
#824=VECTOR ( 'NONE', #32, 1000.000000000000000 ) ;
#831=FACE_BOUND ( 'NONE', #990, .T. ) ;
#835=ORIENTED_EDGE ( 'NONE', *, *, #7339, .T. ) ;
#848=CARTESIAN_POINT ( 'NONE',  ( -25.00000000000000000, 25.00000000000000000, 0.000000000000000000 ) ) ;
#850=CARTESIAN_POINT ( 'NONE',  ( 3.081487911019577803E-31, -25.00000000000000355, 37.50000000000000000 ) ) ;
#871=LINE ( 'NONE', #3326, #586 ) ;
#872=CIRCLE ( 'NONE', #1773, 15.64999999999999680 ) ;
#873=AXIS2_PLACEMENT_3D ( 'NONE', #1597, #2393, #1524 ) ;
#874=ORIENTED_EDGE ( 'NONE', *, *, #4882, .F. ) ;
#875=CARTESIAN_POINT ( 'NONE',  ( -25.00000000000000000, 0.000000000000000000, -12.50000000000000000 ) ) ;
#909=( NAMED_UNIT ( * ) PLANE_ANGLE_UNIT ( ) SI_UNIT ( $, .RADIAN. ) );
#915=LINE ( 'NONE', #3963, #2161 ) ;
#945=AXIS2_PLACEMENT_3D ( 'NONE', #509, #7762, #2993 ) ;
#947=CYLINDRICAL_SURFACE ( 'NONE', #6520, 15.64999999999999680 ) ;
#954=DIRECTION ( 'NONE',  ( 1.000000000000000000, 0.000000000000000000, 0.000000000000000000 ) ) ;
#959=CARTESIAN_POINT ( 'NONE',  ( -25.00000000000000000, 0.000000000000000000, 0.000000000000000000 ) ) ;
#976=AXIS2_PLACEMENT_3D ( 'NONE', #7211, #5517, #4905 ) ;
#990=EDGE_LOOP ( 'NONE', ( #1605, #7138 ) ) ;
#993=AXIS2_PLACEMENT_3D ( 'NONE', #7347, #6223, #1883 ) ;
#995=CARTESIAN_POINT ( 'NONE',  ( -12.50000000000000000, 25.00000000000000355, 3.703880899869785475E-15 ) ) ;
#1014=DIRECTION ( 'NONE',  ( 1.000000000000000000, 0.000000000000000000, 0.000000000000000000 ) ) ;
#1050=CARTESIAN_POINT ( 'NONE',  ( 12.50000000000000000, -25.00000000000000355, 37.50000000000000000 ) ) ;
#1055=ORIENTED_EDGE ( 'NONE', *, *, #323, .F. ) ;
#1056=PLANE ( 'NONE',  #2027 ) ;
#1064=VERTEX_POINT ( 'NONE', #2216 ) ;
#1071=AXIS2_PLACEMENT_3D ( 'NONE', #4710, #5925, #4113 ) ;
#1073=CARTESIAN_POINT ( 'NONE',  ( 15.64999999999999680, 1.916572240665607593E-15, 49.99999999999998579 ) ) ;
#1074=ORIENTED_EDGE ( 'NONE', *, *, #5582, .T. ) ;
#1079=LINE ( 'NONE', #3610, #695 ) ;
#1080=EDGE_CURVE ( 'NONE', #3053, #4682, #410, .T. ) ;
#1084=ORIENTED_EDGE ( 'NONE', *, *, #5520, .F. ) ;
#1106=CARTESIAN_POINT ( 'NONE',  ( 25.00000000000000000, 24.99999999999999289, 50.00000000000000000 ) ) ;
#1115=VERTEX_POINT ( 'NONE', #5906 ) ;
#1129=LINE ( 'NONE', #8, #4910 ) ;
#1146=( LENGTH_UNIT ( ) NAMED_UNIT ( * ) SI_UNIT ( .MILLI., .METRE. ) );
#1159=ORIENTED_EDGE ( 'NONE', *, *, #2526, .T. ) ;
#1167=VERTEX_POINT ( 'NONE', #4810 ) ;
#1172=DIRECTION ( 'NONE',  ( 0.000000000000000000, 0.000000000000000000, -1.000000000000000000 ) ) ;
#1241=CARTESIAN_POINT ( 'NONE',  ( -25.00000000000000000, -25.00000000000000000, 50.00000000000000000 ) ) ;
#1304=LINE ( 'NONE', #1937, #6489 ) ;
#1308=ORIENTED_EDGE ( 'NONE', *, *, #5793, .T. ) ;
#1329=AXIS2_PLACEMENT_3D ( 'NONE', #4466, #3349, #1458 ) ;
#1341=LINE ( 'NONE', #4422, #7355 ) ;
#1343=DIRECTION ( 'NONE',  ( 0.000000000000000000, 1.481552359947913884E-16, -1.000000000000000000 ) ) ;
#1350=DIRECTION ( 'NONE',  ( 0.000000000000000000, 0.000000000000000000, -1.000000000000000000 ) ) ;
#1390=VERTEX_POINT ( 'NONE', #5157 ) ;
#1421=CARTESIAN_POINT ( 'NONE',  ( -25.00000000000000000, 0.000000000000000000, -12.50000000000000000 ) ) ;
#1425=ORIENTED_EDGE ( 'NONE', *, *, #2926, .F. ) ;
#1426=CARTESIAN_POINT ( 'NONE',  ( -15.64999999999999680, 0.000000000000000000, 49.99999999999998579 ) ) ;
#1443=CARTESIAN_POINT ( 'NONE',  ( -11.64999999999996660, 0.000000000000000000, 200.0000000000000000 ) ) ;
#1458=DIRECTION ( 'NONE',  ( 1.000000000000000000, 0.000000000000000000, -0.000000000000000000 ) ) ;
#1459=DIRECTION ( 'NONE',  ( 0.000000000000000000, 0.000000000000000000, -1.000000000000000000 ) ) ;
#1460=ORIENTED_EDGE ( 'NONE', *, *, #4730, .F. ) ;
#1463=ORIENTED_EDGE ( 'NONE', *, *, #2340, .T. ) ;
#1467=AXIS2_PLACEMENT_3D ( 'NONE', #6840, #4467, #1459 ) ;
#1472=CARTESIAN_POINT ( 'NONE',  ( -25.00000000000000000, 0.000000000000000000, 0.000000000000000000 ) ) ;
#1482=FACE_BOUND ( 'NONE', #7374, .T. ) ;
#1504=EDGE_CURVE ( 'NONE', #3922, #3451, #4925, .T. ) ;
#1524=DIRECTION ( 'NONE',  ( 0.000000000000000000, 0.000000000000000000, 1.000000000000000000 ) ) ;
#1528=EDGE_CURVE ( 'NONE', #3115, #3875, #3910, .T. ) ;
#1563=VERTEX_POINT ( 'NONE', #4996 ) ;
#1566=LINE ( 'NONE', #5710, #7424 ) ;
#1574=CARTESIAN_POINT ( 'NONE',  ( 0.000000000000000000, 0.000000000000000000, 200.0000000000000000 ) ) ;
#1585=ORIENTED_EDGE ( 'NONE', *, *, #7514, .T. ) ;
#1597=CARTESIAN_POINT ( 'NONE',  ( -12.50000000000000000, 0.000000000000000000, 0.000000000000000000 ) ) ;
#1605=ORIENTED_EDGE ( 'NONE', *, *, #2734, .T. ) ;
#1630=CARTESIAN_POINT ( 'NONE',  ( -25.00000000000000000, -25.00000000000000000, 0.000000000000000000 ) ) ;
#1650=ORIENTED_EDGE ( 'NONE', *, *, #4197, .F. ) ;
#1651=EDGE_CURVE ( 'NONE', #7564, #4430, #4423, .T. ) ;
#1665=PLANE ( 'NONE',  #4397 ) ;
#1668=PRODUCT_DEFINITION_CONTEXT ( 'detailed design', #3218, 'design' ) ;
#1670=ORIENTED_EDGE ( 'NONE', *, *, #6185, .F. ) ;
#1679=EDGE_LOOP ( 'NONE', ( #277, #5855, #7443, #6655 ) ) ;
#1695=CYLINDRICAL_SURFACE ( 'NONE', #5365, 25.00000000000000000 ) ;
#1701=CARTESIAN_POINT ( 'NONE',  ( 12.50000000000000000, -24.99999999999999645, 3.851859888774471706E-31 ) ) ;
#1738=FACE_OUTER_BOUND ( 'NONE', #5355, .T. ) ;
#1761=ORIENTED_EDGE ( 'NONE', *, *, #1960, .F. ) ;
#1763=CIRCLE ( 'NONE', #6514, 25.00000000000000000 ) ;
#1773=AXIS2_PLACEMENT_3D ( 'NONE', #790, #3241, #5691 ) ;
#1774=CIRCLE ( 'NONE', #114, 15.64999999999999680 ) ;
#1778=CARTESIAN_POINT ( 'NONE',  ( 12.50000000000000000, -24.99999999999999645, -3.235013004037443297E-15 ) ) ;
#1799=ORIENTED_EDGE ( 'NONE', *, *, #4197, .T. ) ;
#1801=DIRECTION ( 'NONE',  ( 1.000000000000000000, 0.000000000000000000, 0.000000000000000000 ) ) ;
#1802=EDGE_CURVE ( 'NONE', #2333, #7620, #5392, .T. ) ;
#1814=DIRECTION ( 'NONE',  ( -0.7071067811865474617, 0.000000000000000000, -0.7071067811865474617 ) ) ;
#1830=VERTEX_POINT ( 'NONE', #5512 ) ;
#1853=CARTESIAN_POINT ( 'NONE',  ( 25.00000000000000000, 0.000000000000000000, 0.000000000000000000 ) ) ;
#1862=CARTESIAN_POINT ( 'NONE',  ( 25.00000000000000000, 0.000000000000000000, 0.000000000000000000 ) ) ;
#1863=EDGE_CURVE ( 'NONE', #3875, #6273, #6600, .T. ) ;
#1867=VERTEX_POINT ( 'NONE', #1701 ) ;
#1883=DIRECTION ( 'NONE',  ( 0.000000000000000000, 0.000000000000000000, 1.000000000000000000 ) ) ;
#1913=ORIENTED_EDGE ( 'NONE', *, *, #717, .T. ) ;
#1924=CARTESIAN_POINT ( 'NONE',  ( -12.50000000000000000, 0.000000000000000000, 0.000000000000000000 ) ) ;
#1927=PRODUCT_CONTEXT ( 'NONE', #3162, 'mechanical' ) ;
#1937=CARTESIAN_POINT ( 'NONE',  ( 25.00000000000000000, -25.00000000000000000, 50.00000000000000000 ) ) ;
#1955=CARTESIAN_POINT ( 'NONE',  ( -25.00000000000000000, -25.00000000000000000, 50.00000000000000000 ) ) ;
#1960=EDGE_CURVE ( 'NONE', #5119, #107, #6232, .T. ) ;
#1984=DIRECTION ( 'NONE',  ( -0.000000000000000000, -0.000000000000000000, -1.000000000000000000 ) ) ;
#2021=AXIS2_PLACEMENT_3D ( 'NONE', #5798, #816, #2140 ) ;
#2027=AXIS2_PLACEMENT_3D ( 'NONE', #1778, #3509, #4222 ) ;
#2029=ORIENTED_EDGE ( 'NONE', *, *, #6398, .F. ) ;
#2034=AXIS2_PLACEMENT_3D ( 'NONE', #1924, #5461, #7389 ) ;
#2071=FACE_OUTER_BOUND ( 'NONE', #4884, .T. ) ;
#2073=SHAPE_REPRESENTATION ( 'Connector', ( #5785 ), #5655 ) ;
#2082=ADVANCED_FACE ( 'NONE', ( #327 ), #2740, .F. ) ;
#2090=CLOSED_SHELL ( 'NONE', ( #7775, #554, #5262, #7013, #7207, #2134, #3615, #3573, #3328, #375, #6010, #5268, #2334, #569, #598, #6964, #225, #5768, #2634, #2082, #5641 ) ) ;
#2107=ORIENTED_EDGE ( 'NONE', *, *, #1651, .T. ) ;
#2134=ADVANCED_FACE ( 'NONE', ( #6512 ), #7754, .F. ) ;
#2135=VECTOR ( 'NONE', #533, 1000.000000000000000 ) ;
#2140=DIRECTION ( 'NONE',  ( 0.000000000000000000, 0.000000000000000000, -1.000000000000000000 ) ) ;
#2155=( GEOMETRIC_REPRESENTATION_CONTEXT ( 3 ) GLOBAL_UNCERTAINTY_ASSIGNED_CONTEXT ( ( #6961 ) ) GLOBAL_UNIT_ASSIGNED_CONTEXT ( ( #4632, #909, #3359 ) ) REPRESENTATION_CONTEXT ( 'NONE', 'WORKASPACE' ) );
#2161=VECTOR ( 'NONE', #7054, 1000.000000000000000 ) ;
#2169=CONICAL_SURFACE ( 'NONE', #5236, 11.64999999999996660, 0.7853981633974482790 ) ;
#2171=ORIENTED_EDGE ( 'NONE', *, *, #5582, .F. ) ;
#2187=EDGE_CURVE ( 'NONE', #4661, #2323, #1129, .T. ) ;
#2203=DIRECTION ( 'NONE',  ( 0.000000000000000000, 0.000000000000000000, -1.000000000000000000 ) ) ;
#2216=CARTESIAN_POINT ( 'NONE',  ( 25.00000000000000000, 0.000000000000000000, -12.50000000000000000 ) ) ;
#2240=ORIENTED_EDGE ( 'NONE', *, *, #4119, .F. ) ;
#2305=PLANE ( 'NONE',  #5557 ) ;
#2320=PLANE ( 'NONE',  #5560 ) ;
#2323=VERTEX_POINT ( 'NONE', #1050 ) ;
#2326=FACE_OUTER_BOUND ( 'NONE', #3099, .T. ) ;
#2333=VERTEX_POINT ( 'NONE', #459 ) ;
#2334=ADVANCED_FACE ( 'NONE', ( #5343 ), #2305, .T. ) ;
#2340=EDGE_CURVE ( 'NONE', #6273, #1867, #2359, .T. ) ;
#2346=DIRECTION ( 'NONE',  ( 1.000000000000000000, 0.000000000000000000, 0.000000000000000000 ) ) ;
#2351=DIRECTION ( 'NONE',  ( 1.000000000000000000, 0.000000000000000000, 0.000000000000000000 ) ) ;
#2358=EDGE_CURVE ( 'NONE', #2323, #1867, #4294, .T. ) ;
#2359=CIRCLE ( 'NONE', #3252, 25.00000000000000000 ) ;
#2372=DIRECTION ( 'NONE',  ( -1.000000000000000000, -0.000000000000000000, -0.000000000000000000 ) ) ;
#2375=DIRECTION ( 'NONE',  ( 0.000000000000000000, -1.000000000000000000, 0.000000000000000000 ) ) ;
#2384=DIRECTION ( 'NONE',  ( 1.000000000000000000, 0.000000000000000000, 0.000000000000000000 ) ) ;
#2393=DIRECTION ( 'NONE',  ( 1.000000000000000000, 0.000000000000000000, -0.000000000000000000 ) ) ;
#2398=CARTESIAN_POINT ( 'NONE',  ( 12.50000000000000000, 24.99999999999999645, 37.50000000000000711 ) ) ;
#2404=ORIENTED_EDGE ( 'NONE', *, *, #2858, .T. ) ;
#2412=CIRCLE ( 'NONE', #2936, 15.64999999999999680 ) ;
#2414=LINE ( 'NONE', #7192, #2135 ) ;
#2434=DIRECTION ( 'NONE',  ( 1.000000000000000000, 0.000000000000000000, 0.000000000000000000 ) ) ;
#2437=ORIENTED_EDGE ( 'NONE', *, *, #2675, .T. ) ;
#2446=LINE ( 'NONE', #3845, #824 ) ;
#2475=ORIENTED_EDGE ( 'NONE', *, *, #2928, .T. ) ;
#2526=EDGE_CURVE ( 'NONE', #1390, #1064, #4914, .T. ) ;
#2529=CARTESIAN_POINT ( 'NONE',  ( -25.00000000000000000, 24.99999999999999289, 50.00000000000000000 ) ) ;
#2543=VECTOR ( 'NONE', #7633, 1000.000000000000000 ) ;
#2567=DIRECTION ( 'NONE',  ( 0.000000000000000000, 0.000000000000000000, 1.000000000000000000 ) ) ;
#2589=EDGE_LOOP ( 'NONE', ( #138, #6963 ) ) ;
#2620=EDGE_LOOP ( 'NONE', ( #5513, #2240, #835, #3415 ) ) ;
#2630=ORIENTED_EDGE ( 'NONE', *, *, #236, .F. ) ;
#2634=ADVANCED_FACE ( 'NONE', ( #6982, #1482 ), #320, .F. ) ;
#2647=ORIENTED_EDGE ( 'NONE', *, *, #1651, .F. ) ;
#2652=ORIENTED_EDGE ( 'NONE', *, *, #4929, .F. ) ;
#2660=AXIS2_PLACEMENT_3D ( 'NONE', #7289, #6083, #4189 ) ;
#2661=EDGE_LOOP ( 'NONE', ( #407, #7170, #5918, #2029 ) ) ;
#2667=DIRECTION ( 'NONE',  ( -1.000000000000000000, 0.000000000000000000, 0.000000000000000000 ) ) ;
#2671=ORIENTED_EDGE ( 'NONE', *, *, #4811, .F. ) ;
#2674=ORIENTED_EDGE ( 'NONE', *, *, #7522, .T. ) ;
#2675=EDGE_CURVE ( 'NONE', #646, #5119, #1079, .T. ) ;
#2713=ORIENTED_EDGE ( 'NONE', *, *, #3081, .F. ) ;
#2733=ORIENTED_EDGE ( 'NONE', *, *, #4929, .T. ) ;
#2734=EDGE_CURVE ( 'NONE', #7564, #6254, #3269, .T. ) ;
#2740=PLANE ( 'NONE',  #5038 ) ;
#2764=ORIENTED_EDGE ( 'NONE', *, *, #3220, .T. ) ;
#2771=DIRECTION ( 'NONE',  ( 0.000000000000000000, 0.000000000000000000, 1.000000000000000000 ) ) ;
#2778=LINE ( 'NONE', #848, #4332 ) ;
#2822=DIRECTION ( 'NONE',  ( 0.000000000000000000, -1.387778780781445676E-16, 1.000000000000000000 ) ) ;
#2846=FACE_OUTER_BOUND ( 'NONE', #5534, .T. ) ;
#2852=DIRECTION ( 'NONE',  ( 1.000000000000000000, 0.000000000000000000, 0.000000000000000000 ) ) ;
#2857=DIRECTION ( 'NONE',  ( -1.000000000000000000, -0.000000000000000000, 0.000000000000000000 ) ) ;
#2858=EDGE_CURVE ( 'NONE', #5119, #6483, #3806, .T. ) ;
#2886=CARTESIAN_POINT ( 'NONE',  ( -25.00000000000000000, 25.00000000000000000, 0.000000000000000000 ) ) ;
#2890=CIRCLE ( 'NONE', #4664, 25.00000000000000000 ) ;
#2917=ORIENTED_EDGE ( 'NONE', *, *, #6151, .T. ) ;
#2922=CIRCLE ( 'NONE', #7144, 12.50000000000000000 ) ;
#2926=EDGE_CURVE ( 'NONE', #6684, #3810, #5036, .T. ) ;
#2927=AXIS2_PLACEMENT_3D ( 'NONE', #4400, #3333, #2567 ) ;
#2928=EDGE_CURVE ( 'NONE', #221, #1390, #2446, .T. ) ;
#2933=ORIENTED_EDGE ( 'NONE', *, *, #1960, .T. ) ;
#2936=AXIS2_PLACEMENT_3D ( 'NONE', #3231, #664, #5553 ) ;
#2948=CARTESIAN_POINT ( 'NONE',  ( -25.00000000000000000, -25.00000000000000000, 50.00000000000000000 ) ) ;
#2956=FACE_BOUND ( 'NONE', #5681, .T. ) ;
#2958=ORIENTED_EDGE ( 'NONE', *, *, #147, .T. ) ;
#2993=DIRECTION ( 'NONE',  ( 0.000000000000000000, -1.387778780781445676E-16, 1.000000000000000000 ) ) ;
#3033=AXIS2_PLACEMENT_3D ( 'NONE', #5371, #2852, #2203 ) ;
#3040=DIRECTION ( 'NONE',  ( 1.000000000000000000, 0.000000000000000000, 0.000000000000000000 ) ) ;
#3041=CARTESIAN_POINT ( 'NONE',  ( 12.50000000000000355, 1.530808498934191521E-15, 12.50000000000000000 ) ) ;
#3053=VERTEX_POINT ( 'NONE', #3920 ) ;
#3081=EDGE_CURVE ( 'NONE', #6638, #3115, #871, .T. ) ;
#3099=EDGE_LOOP ( 'NONE', ( #157, #1074, #1585, #5931 ) ) ;
#3107=DIRECTION ( 'NONE',  ( 0.000000000000000000, 1.481552359947913884E-16, -1.000000000000000000 ) ) ;
#3115=VERTEX_POINT ( 'NONE', #2398 ) ;
#3139=CARTESIAN_POINT ( 'NONE',  ( 25.00000000000000000, -25.00000000000000000, 50.00000000000000000 ) ) ;
#3141=VECTOR ( 'NONE', #1343, 1000.000000000000000 ) ;
#3152=ORIENTED_EDGE ( 'NONE', *, *, #5419, .F. ) ;
#3160=CARTESIAN_POINT ( 'NONE',  ( 11.64999999999996660, 1.426713521006662464E-15, 200.0000000000000000 ) ) ;
#3162=APPLICATION_CONTEXT ( 'automotive_design' ) ;
#3187=DIRECTION ( 'NONE',  ( 1.000000000000000000, 0.000000000000000000, 0.000000000000000000 ) ) ;
#3188=DIRECTION ( 'NONE',  ( 0.000000000000000000, 0.000000000000000000, -1.000000000000000000 ) ) ;
#3218=APPLICATION_CONTEXT ( 'automotive_design' ) ;
#3220=EDGE_CURVE ( 'NONE', #3875, #7818, #3487, .T. ) ;
#3231=CARTESIAN_POINT ( 'NONE',  ( 0.000000000000000000, 0.000000000000000000, 49.99999999999998579 ) ) ;
#3239=CARTESIAN_POINT ( 'NONE',  ( 12.50000000000000000, 25.00000000000000355, 7.703719777548943412E-31 ) ) ;
#3241=DIRECTION ( 'NONE',  ( 0.000000000000000000, 0.000000000000000000, -1.000000000000000000 ) ) ;
#3243=EDGE_LOOP ( 'NONE', ( #7505, #5769, #4946, #2647 ) ) ;
#3252=AXIS2_PLACEMENT_3D ( 'NONE', #7272, #6668, #1172 ) ;
#3260=ADVANCED_BREP_SHAPE_REPRESENTATION ( '', ( #7010, #5785 ), #5655 ) ;
#3269=CIRCLE ( 'NONE', #3655, 12.50000000000000000 ) ;
#3275=VECTOR ( 'NONE', #5321, 1000.000000000000000 ) ;
#3309=CARTESIAN_POINT ( 'NONE',  ( 12.50000000000000000, -25.00000000000000355, 37.50000000000000000 ) ) ;
#3326=CARTESIAN_POINT ( 'NONE',  ( 3.081487911019577803E-31, 24.99999999999999645, 37.50000000000000711 ) ) ;
#3328=ADVANCED_FACE ( 'NONE', ( #4911 ), #595, .T. ) ;
#3333=DIRECTION ( 'NONE',  ( 1.000000000000000000, 0.000000000000000000, -0.000000000000000000 ) ) ;
#3343=DIRECTION ( 'NONE',  ( 0.7071067811865474617, 8.659560562354932858E-17, -0.7071067811865474617 ) ) ;
#3346=ORIENTED_EDGE ( 'NONE', *, *, #5324, .T. ) ;
#3348=DIRECTION ( 'NONE',  ( 1.000000000000000000, 0.000000000000000000, 0.000000000000000000 ) ) ;
#3349=DIRECTION ( 'NONE',  ( 0.000000000000000000, 0.000000000000000000, 1.000000000000000000 ) ) ;
#3359=( NAMED_UNIT ( * ) SI_UNIT ( $, .STERADIAN. ) SOLID_ANGLE_UNIT ( ) );
#3395=VECTOR ( 'NONE', #6289, 1000.000000000000000 ) ;
#3402=AXIS2_PLACEMENT_3D ( 'NONE', #5559, #1984, #7330 ) ;
#3406=EDGE_CURVE ( 'NONE', #3053, #2333, #6806, .T. ) ;
#3415=ORIENTED_EDGE ( 'NONE', *, *, #6938, .F. ) ;
#3451=VERTEX_POINT ( 'NONE', #6513 ) ;
#3474=CARTESIAN_POINT ( 'NONE',  ( 25.00000000000000000, 25.00000000000000000, 0.000000000000000000 ) ) ;
#3476=CYLINDRICAL_SURFACE ( 'NONE', #5301, 25.00000000000000000 ) ;
#3487=LINE ( 'NONE', #2886, #3275 ) ;
#3497=EDGE_LOOP ( 'NONE', ( #6730, #6218, #2764, #6291 ) ) ;
#3504=CARTESIAN_POINT ( 'NONE',  ( -25.00000000000000000, 0.000000000000000000, 0.000000000000000000 ) ) ;
#3509=DIRECTION ( 'NONE',  ( 1.000000000000000000, 0.000000000000000000, 0.000000000000000000 ) ) ;
#3523=VECTOR ( 'NONE', #6893, 1000.000000000000000 ) ;
#3539=CARTESIAN_POINT ( 'NONE',  ( 12.50000000000000355, 0.000000000000000000, -25.00000000000000000 ) ) ;
#3546=ORIENTED_EDGE ( 'NONE', *, *, #6938, .T. ) ;
#3559=ORIENTED_EDGE ( 'NONE', *, *, #2858, .F. ) ;
#3573=ADVANCED_FACE ( 'NONE', ( #5245 ), #7056, .T. ) ;
#3610=CARTESIAN_POINT ( 'NONE',  ( -25.00000000000000000, 24.99999999999999289, 50.00000000000000000 ) ) ;
#3615=ADVANCED_FACE ( 'NONE', ( #2326 ), #4721, .F. ) ;
#3617=AXIS2_PLACEMENT_3D ( 'NONE', #499, #7228, #1014 ) ;
#3655=AXIS2_PLACEMENT_3D ( 'NONE', #5408, #1801, #4244 ) ;
#3670=CARTESIAN_POINT ( 'NONE',  ( -12.50000000000000000, 0.000000000000000000, -12.50000000000000000 ) ) ;
#3715=CIRCLE ( 'NONE', #2034, 25.00000000000000000 ) ;
#3720=ORIENTED_EDGE ( 'NONE', *, *, #6076, .F. ) ;
#3766=DIRECTION ( 'NONE',  ( -1.000000000000000000, 0.000000000000000000, 0.000000000000000000 ) ) ;
#3776=DIRECTION ( 'NONE',  ( 1.000000000000000000, 0.000000000000000000, 0.000000000000000000 ) ) ;
#3806=LINE ( 'NONE', #1241, #3395 ) ;
#3810=VERTEX_POINT ( 'NONE', #1426 ) ;
#3823=AXIS2_PLACEMENT_3D ( 'NONE', #1472, #304, #435 ) ;
#3831=DIRECTION ( 'NONE',  ( 0.000000000000000000, 0.000000000000000000, -1.000000000000000000 ) ) ;
#3833=DIRECTION ( 'NONE',  ( 1.000000000000000000, 0.000000000000000000, 0.000000000000000000 ) ) ;
#3845=CARTESIAN_POINT ( 'NONE',  ( -25.00000000000000000, 1.530808498934191521E-15, 12.50000000000000000 ) ) ;
#3856=CARTESIAN_POINT ( 'NONE',  ( 12.50000000000000000, -24.99999999999999645, -3.235013004037443297E-15 ) ) ;
#3858=PRODUCT ( 'Connector', 'Connector', '', ( #1927 ) ) ;
#3871=DIRECTION ( 'NONE',  ( 1.000000000000000000, 0.000000000000000000, 0.000000000000000000 ) ) ;
#3875=VERTEX_POINT ( 'NONE', #3239 ) ;
#3889=CARTESIAN_POINT ( 'NONE',  ( 25.00000000000000000, 0.000000000000000000, 0.000000000000000000 ) ) ;
#3906=LINE ( 'NONE', #3474, #4176 ) ;
#3907=LINE ( 'NONE', #7075, #5616 ) ;
#3910=LINE ( 'NONE', #6281, #3141 ) ;
#3916=EDGE_LOOP ( 'NONE', ( #4595, #6602, #1650, #3559, #2933, #4285, #3983, #5484 ) ) ;
#3920=CARTESIAN_POINT ( 'NONE',  ( 11.64999999999996660, 1.671642880836134930E-15, 200.0000000000000000 ) ) ;
#3922=VERTEX_POINT ( 'NONE', #7007 ) ;
#3930=CARTESIAN_POINT ( 'NONE',  ( -25.00000000000000000, 0.000000000000000000, 0.000000000000000000 ) ) ;
#3931=DIRECTION ( 'NONE',  ( 1.000000000000000000, 0.000000000000000000, 0.000000000000000000 ) ) ;
#3943=ORIENTED_EDGE ( 'NONE', *, *, #4882, .T. ) ;
#3951=ORIENTED_EDGE ( 'NONE', *, *, #323, .T. ) ;
#3963=CARTESIAN_POINT ( 'NONE',  ( -25.00000000000000000, 0.000000000000000000, -12.50000000000000000 ) ) ;
#3983=ORIENTED_EDGE ( 'NONE', *, *, #4811, .T. ) ;
#4003=DIRECTION ( 'NONE',  ( 0.000000000000000000, 0.000000000000000000, -1.000000000000000000 ) ) ;
#4020=DIRECTION ( 'NONE',  ( 0.000000000000000000, 0.000000000000000000, -1.000000000000000000 ) ) ;
#4039=VERTEX_POINT ( 'NONE', #4829 ) ;
#4041=ORIENTED_EDGE ( 'NONE', *, *, #1863, .T. ) ;
#4048=CARTESIAN_POINT ( 'NONE',  ( -12.50000000000000000, 24.99999999999999645, 37.50000000000000711 ) ) ;
#4060=VECTOR ( 'NONE', #3776, 1000.000000000000000 ) ;
#4072=AXIS2_PLACEMENT_3D ( 'NONE', #1574, #4020, #2667 ) ;
#4077=DIRECTION ( 'NONE',  ( -0.000000000000000000, -0.000000000000000000, -1.000000000000000000 ) ) ;
#4083=VECTOR ( 'NONE', #954, 1000.000000000000000 ) ;
#4089=ORIENTED_EDGE ( 'NONE', *, *, #6858, .F. ) ;
#4104=CARTESIAN_POINT ( 'NONE',  ( -25.00000000000000000, 0.000000000000000000, 0.000000000000000000 ) ) ;
#4110=CARTESIAN_POINT ( 'NONE',  ( 0.000000000000000000, 0.000000000000000000, 0.000000000000000000 ) ) ;
#4113=DIRECTION ( 'NONE',  ( 1.000000000000000000, 0.000000000000000000, 0.000000000000000000 ) ) ;
#4119=EDGE_CURVE ( 'NONE', #4682, #3053, #6745, .T. ) ;
#4129=DIRECTION ( 'NONE',  ( 0.000000000000000000, 0.000000000000000000, -1.000000000000000000 ) ) ;
#4131=DIRECTION ( 'NONE',  ( 1.000000000000000000, -1.232595164407830946E-32, -1.710569414459005214E-48 ) ) ;
#4176=VECTOR ( 'NONE', #5137, 1000.000000000000000 ) ;
#4179=DIRECTION ( 'NONE',  ( -0.000000000000000000, 0.000000000000000000, 1.000000000000000000 ) ) ;
#4181=DIRECTION ( 'NONE',  ( 0.000000000000000000, 0.000000000000000000, -1.000000000000000000 ) ) ;
#4186=DIRECTION ( 'NONE',  ( 0.000000000000000000, 0.000000000000000000, 1.000000000000000000 ) ) ;
#4189=DIRECTION ( 'NONE',  ( 0.000000000000000000, 0.000000000000000000, -1.000000000000000000 ) ) ;
#4197=EDGE_CURVE ( 'NONE', #6483, #1563, #1304, .T. ) ;
#4202=ORIENTED_EDGE ( 'NONE', *, *, #4306, .T. ) ;
#4222=DIRECTION ( 'NONE',  ( 0.000000000000000000, 0.000000000000000000, -1.000000000000000000 ) ) ;
#4224=DIRECTION ( 'NONE',  ( -0.000000000000000000, -0.000000000000000000, -1.000000000000000000 ) ) ;
#4227=ORIENTED_EDGE ( 'NONE', *, *, #5158, .F. ) ;
#4244=DIRECTION ( 'NONE',  ( 0.000000000000000000, 0.000000000000000000, -1.000000000000000000 ) ) ;
#4274=CARTESIAN_POINT ( 'NONE',  ( 0.000000000000000000, 0.000000000000000000, 200.0000000000000000 ) ) ;
#4285=ORIENTED_EDGE ( 'NONE', *, *, #7575, .T. ) ;
#4294=LINE ( 'NONE', #3856, #6713 ) ;
#4306=EDGE_CURVE ( 'NONE', #7818, #36, #3906, .T. ) ;
#4323=EDGE_LOOP ( 'NONE', ( #2733, #5759, #2674, #4089, #2671 ) ) ;
#4332=VECTOR ( 'NONE', #6913, 1000.000000000000000 ) ;
#4337=CARTESIAN_POINT ( 'NONE',  ( -25.00000000000000000, 0.000000000000000000, 0.000000000000000000 ) ) ;
#4347=CARTESIAN_POINT ( 'NONE',  ( 25.00000000000000000, 0.000000000000000000, 0.000000000000000000 ) ) ;
#4349=VERTEX_POINT ( 'NONE', #5263 ) ;
#4363=ORIENTED_EDGE ( 'NONE', *, *, #126, .F. ) ;
#4369=SHAPE_DEFINITION_REPRESENTATION ( #205, #2073 ) ;
#4397=AXIS2_PLACEMENT_3D ( 'NONE', #6559, #4179, #2346 ) ;
#4400=CARTESIAN_POINT ( 'NONE',  ( -12.50000000000000000, 0.000000000000000000, 0.000000000000000000 ) ) ;
#4422=CARTESIAN_POINT ( 'NONE',  ( -25.00000000000000000, 1.530808498934191521E-15, 12.50000000000000000 ) ) ;
#4423=LINE ( 'NONE', #1421, #6980 ) ;
#4430=VERTEX_POINT ( 'NONE', #3670 ) ;
#4435=CARTESIAN_POINT ( 'NONE',  ( -15.64999999999999680, 0.000000000000000000, 200.0000000000000000 ) ) ;
#4445=CIRCLE ( 'NONE', #2927, 12.50000000000000000 ) ;
#4450=CIRCLE ( 'NONE', #2021, 12.50000000000000000 ) ;
#4455=MECHANICAL_DESIGN_GEOMETRIC_PRESENTATION_REPRESENTATION('',(#4714),#2155);
#4466=CARTESIAN_POINT ( 'NONE',  ( 0.000000000000000000, 0.000000000000000000, 200.0000000000000000 ) ) ;
#4467=DIRECTION ( 'NONE',  ( 1.000000000000000000, 0.000000000000000000, 0.000000000000000000 ) ) ;
#4519=DIRECTION ( 'NONE',  ( 0.000000000000000000, -1.481552359947913884E-16, 1.000000000000000000 ) ) ;
#4526=CIRCLE ( 'NONE', #5945, 25.00000000000000000 ) ;
#4595=ORIENTED_EDGE ( 'NONE', *, *, #2358, .T. ) ;
#4632=( LENGTH_UNIT ( ) NAMED_UNIT ( * ) SI_UNIT ( .MILLI., .METRE. ) );
#4649=VECTOR ( 'NONE', #808, 1000.000000000000000 ) ;
#4654=DIRECTION ( 'NONE',  ( 1.000000000000000000, 0.000000000000000000, 0.000000000000000000 ) ) ;
#4659=FACE_OUTER_BOUND ( 'NONE', #6687, .T. ) ;
#4661=VERTEX_POINT ( 'NONE', #7067 ) ;
#4664=AXIS2_PLACEMENT_3D ( 'NONE', #1853, #6754, #3188 ) ;
#4672=DIRECTION ( 'NONE',  ( -1.000000000000000000, 0.000000000000000000, 0.000000000000000000 ) ) ;
#4682=VERTEX_POINT ( 'NONE', #1443 ) ;
#4710=CARTESIAN_POINT ( 'NONE',  ( 0.000000000000000000, 0.000000000000000000, 49.99999999999998579 ) ) ;
#4714=STYLED_ITEM('',(#7948),#7010);
#4721=CYLINDRICAL_SURFACE ( 'NONE', #6482, 12.50000000000000000 ) ;
#4730=EDGE_CURVE ( 'NONE', #4039, #221, #2922, .T. ) ;
#4731=DIRECTION ( 'NONE',  ( 1.000000000000000000, 0.000000000000000000, 0.000000000000000000 ) ) ;
#4738=EDGE_CURVE ( 'NONE', #6273, #1167, #5941, .T. ) ;
#4743=CARTESIAN_POINT ( 'NONE',  ( 0.000000000000000000, 0.000000000000000000, 195.9999999999999716 ) ) ;
#4745=CARTESIAN_POINT ( 'NONE',  ( 12.50000000000000355, 0.000000000000000000, 0.000000000000000000 ) ) ;
#4760=DIRECTION ( 'NONE',  ( 1.000000000000000000, 0.000000000000000000, 0.000000000000000000 ) ) ;
#4776=VECTOR ( 'NONE', #7844, 1000.000000000000000 ) ;
#4810=CARTESIAN_POINT ( 'NONE',  ( 25.00000000000000000, 0.000000000000000000, -25.00000000000000000 ) ) ;
#4811=EDGE_CURVE ( 'NONE', #1830, #4661, #2414, .T. ) ;
#4812=DIRECTION ( 'NONE',  ( 0.000000000000000000, -0.000000000000000000, -1.000000000000000000 ) ) ;
#4819=FACE_BOUND ( 'NONE', #6055, .T. ) ;
#4829=CARTESIAN_POINT ( 'NONE',  ( 12.50000000000000355, 0.000000000000000000, -12.50000000000000000 ) ) ;
#4838=ORIENTED_EDGE ( 'NONE', *, *, #126, .T. ) ;
#4853=CARTESIAN_POINT ( 'NONE',  ( -25.00000000000000000, 0.000000000000000000, -25.00000000000000000 ) ) ;
#4867=FACE_OUTER_BOUND ( 'NONE', #2661, .T. ) ;
#4868=DIRECTION ( 'NONE',  ( 0.000000000000000000, 0.000000000000000000, -1.000000000000000000 ) ) ;
#4882=EDGE_CURVE ( 'NONE', #646, #36, #80, .T. ) ;
#4884=EDGE_LOOP ( 'NONE', ( #5196, #1761, #6157, #3720, #5008 ) ) ;
#4905=DIRECTION ( 'NONE',  ( 1.000000000000000000, 0.000000000000000000, 0.000000000000000000 ) ) ;
#4910=VECTOR ( 'NONE', #4131, 1000.000000000000000 ) ;
#4911=FACE_OUTER_BOUND ( 'NONE', #7205, .T. ) ;
#4914=CIRCLE ( 'NONE', #182, 12.50000000000000000 ) ;
#4925=CIRCLE ( 'NONE', #1467, 25.00000000000000000 ) ;
#4929=EDGE_CURVE ( 'NONE', #1830, #4349, #5481, .T. ) ;
#4946=ORIENTED_EDGE ( 'NONE', *, *, #5158, .T. ) ;
#4952=ORIENTED_EDGE ( 'NONE', *, *, #4738, .T. ) ;
#4996=CARTESIAN_POINT ( 'NONE',  ( 25.00000000000000000, -25.00000000000000000, 0.000000000000000000 ) ) ;
#5008=ORIENTED_EDGE ( 'NONE', *, *, #1504, .F. ) ;
#5028=ORIENTED_EDGE ( 'NONE', *, *, #7514, .F. ) ;
#5035=CARTESIAN_POINT ( 'NONE',  ( -12.50000000000000000, -25.00000000000000355, 37.50000000000000000 ) ) ;
#5036=LINE ( 'NONE', #4435, #3523 ) ;
#5038=AXIS2_PLACEMENT_3D ( 'NONE', #850, #2822, #7588 ) ;
#5053=DIRECTION ( 'NONE',  ( 1.000000000000000000, 0.000000000000000000, 0.000000000000000000 ) ) ;
#5068=VERTEX_POINT ( 'NONE', #762 ) ;
#5080=VECTOR ( 'NONE', #4731, 1000.000000000000000 ) ;
#5087=DIRECTION ( 'NONE',  ( 0.000000000000000000, 0.000000000000000000, -1.000000000000000000 ) ) ;
#5119=VERTEX_POINT ( 'NONE', #1955 ) ;
#5130=DIRECTION ( 'NONE',  ( 1.000000000000000000, 0.000000000000000000, 0.000000000000000000 ) ) ;
#5137=DIRECTION ( 'NONE',  ( 0.000000000000000000, -1.387778780781445676E-16, 1.000000000000000000 ) ) ;
#5148=LINE ( 'NONE', #5035, #5874 ) ;
#5157=CARTESIAN_POINT ( 'NONE',  ( 25.00000000000000000, 1.530808498934191521E-15, 12.50000000000000000 ) ) ;
#5158=EDGE_CURVE ( 'NONE', #1115, #4430, #4445, .T. ) ;
#5196=ORIENTED_EDGE ( 'NONE', *, *, #6570, .F. ) ;
#5235=CARTESIAN_POINT ( 'NONE',  ( 25.00000000000000000, 24.99999999999999289, 50.00000000000000000 ) ) ;
#5236=AXIS2_PLACEMENT_3D ( 'NONE', #4274, #1350, #3766 ) ;
#5243=CARTESIAN_POINT ( 'NONE',  ( -25.00000000000000000, -25.00000000000000000, 0.000000000000000000 ) ) ;
#5245=FACE_OUTER_BOUND ( 'NONE', #3497, .T. ) ;
#5262=ADVANCED_FACE ( 'NONE', ( #6680 ), #314, .F. ) ;
#5263=CARTESIAN_POINT ( 'NONE',  ( -12.50000000000000000, 0.000000000000000000, -25.00000000000000000 ) ) ;
#5268=ADVANCED_FACE ( 'NONE', ( #4867 ), #5815, .T. ) ;
#5291=ORIENTED_EDGE ( 'NONE', *, *, #6076, .T. ) ;
#5297=AXIS2_PLACEMENT_3D ( 'NONE', #6466, #5752, #256 ) ;
#5301=AXIS2_PLACEMENT_3D ( 'NONE', #4104, #2384, #5916 ) ;
#5321=DIRECTION ( 'NONE',  ( 1.000000000000000000, 0.000000000000000000, 0.000000000000000000 ) ) ;
#5324=EDGE_CURVE ( 'NONE', #4430, #1115, #5869, .T. ) ;
#5328=ORIENTED_EDGE ( 'NONE', *, *, #7575, .F. ) ;
#5336=ORIENTED_EDGE ( 'NONE', *, *, #4730, .T. ) ;
#5343=FACE_OUTER_BOUND ( 'NONE', #3916, .T. ) ;
#5352=DIRECTION ( 'NONE',  ( -1.000000000000000000, -0.000000000000000000, -0.000000000000000000 ) ) ;
#5355=EDGE_LOOP ( 'NONE', ( #250, #2917, #2652, #5328 ) ) ;
#5365=AXIS2_PLACEMENT_3D ( 'NONE', #3504, #4654, #376 ) ;
#5370=VECTOR ( 'NONE', #1814, 1000.000000000000114 ) ;
#5371=CARTESIAN_POINT ( 'NONE',  ( -25.00000000000000000, 0.000000000000000000, 0.000000000000000000 ) ) ;
#5379=ORIENTED_EDGE ( 'NONE', *, *, #1802, .F. ) ;
#5392=LINE ( 'NONE', #7838, #564 ) ;
#5408=CARTESIAN_POINT ( 'NONE',  ( -25.00000000000000000, 0.000000000000000000, 0.000000000000000000 ) ) ;
#5419=EDGE_CURVE ( 'NONE', #7620, #3810, #2412, .T. ) ;
#5435=ORIENTED_EDGE ( 'NONE', *, *, #3081, .T. ) ;
#5461=DIRECTION ( 'NONE',  ( 1.000000000000000000, 0.000000000000000000, -0.000000000000000000 ) ) ;
#5481=CIRCLE ( 'NONE', #993, 25.00000000000000000 ) ;
#5484=ORIENTED_EDGE ( 'NONE', *, *, #2187, .T. ) ;
#5512=CARTESIAN_POINT ( 'NONE',  ( -12.50000000000000000, -24.99999999999999645, 3.851859888774471706E-31 ) ) ;
#5513=ORIENTED_EDGE ( 'NONE', *, *, #3406, .F. ) ;
#5517=DIRECTION ( 'NONE',  ( 0.000000000000000000, 0.000000000000000000, 1.000000000000000000 ) ) ;
#5520=EDGE_CURVE ( 'NONE', #3451, #5068, #3907, .T. ) ;
#5534=EDGE_LOOP ( 'NONE', ( #1308, #6408, #6976, #1425 ) ) ;
#5553=DIRECTION ( 'NONE',  ( 1.000000000000000000, 0.000000000000000000, 0.000000000000000000 ) ) ;
#5557=AXIS2_PLACEMENT_3D ( 'NONE', #2948, #2375, #4812 ) ;
#5559=CARTESIAN_POINT ( 'NONE',  ( 0.000000000000000000, 0.000000000000000000, 200.0000000000000000 ) ) ;
#5560=AXIS2_PLACEMENT_3D ( 'NONE', #1862, #3833, #21 ) ;
#5572=EDGE_CURVE ( 'NONE', #2323, #3115, #6353, .T. ) ;
#5582=EDGE_CURVE ( 'NONE', #221, #4039, #4450, .T. ) ;
#5616=VECTOR ( 'NONE', #3348, 1000.000000000000000 ) ;
#5622=ORIENTED_EDGE ( 'NONE', *, *, #5572, .T. ) ;
#5641=ADVANCED_FACE ( 'NONE', ( #7041 ), #7534, .T. ) ;
#5655=( GEOMETRIC_REPRESENTATION_CONTEXT ( 3 ) GLOBAL_UNCERTAINTY_ASSIGNED_CONTEXT ( ( #6886 ) ) GLOBAL_UNIT_ASSIGNED_CONTEXT ( ( #1146, #7173, #7722 ) ) REPRESENTATION_CONTEXT ( 'NONE', 'WORKASPACE' ) );
#5676=ORIENTED_EDGE ( 'NONE', *, *, #5324, .F. ) ;
#5681=EDGE_LOOP ( 'NONE', ( #7384, #3152 ) ) ;
#5691=DIRECTION ( 'NONE',  ( 1.000000000000000000, 0.000000000000000000, 0.000000000000000000 ) ) ;
#5695=EDGE_LOOP ( 'NONE', ( #3951, #1913, #4202, #4838, #1799 ) ) ;
#5710=CARTESIAN_POINT ( 'NONE',  ( -25.00000000000000000, 0.000000000000000000, -25.00000000000000000 ) ) ;
#5712=CARTESIAN_POINT ( 'NONE',  ( -25.00000000000000000, -25.00000000000000000, 50.00000000000000000 ) ) ;
#5752=DIRECTION ( 'NONE',  ( 1.000000000000000000, 0.000000000000000000, 0.000000000000000000 ) ) ;
#5754=VECTOR ( 'NONE', #3187, 1000.000000000000000 ) ;
#5759=ORIENTED_EDGE ( 'NONE', *, *, #6398, .T. ) ;
#5768=ADVANCED_FACE ( 'NONE', ( #6673, #4819 ), #1056, .F. ) ;
#5769=ORIENTED_EDGE ( 'NONE', *, *, #236, .T. ) ;
#5783=DIRECTION ( 'NONE',  ( 0.000000000000000000, 0.000000000000000000, -1.000000000000000000 ) ) ;
#5785=AXIS2_PLACEMENT_3D ( 'NONE', #4110, #4186, #2351 ) ;
#5793=EDGE_CURVE ( 'NONE', #6684, #2333, #1774, .T. ) ;
#5798=CARTESIAN_POINT ( 'NONE',  ( 12.50000000000000355, 0.000000000000000000, 0.000000000000000000 ) ) ;
#5815=CYLINDRICAL_SURFACE ( 'NONE', #2660, 25.00000000000000000 ) ;
#5855=ORIENTED_EDGE ( 'NONE', *, *, #3406, .T. ) ;
#5857=DIRECTION ( 'NONE',  ( 0.000000000000000000, 0.000000000000000000, -1.000000000000000000 ) ) ;
#5868=CIRCLE ( 'NONE', #7302, 12.50000000000000000 ) ;
#5869=CIRCLE ( 'NONE', #873, 12.50000000000000000 ) ;
#5874=VECTOR ( 'NONE', #188, 1000.000000000000000 ) ;
#5885=EDGE_CURVE ( 'NONE', #1867, #1563, #7470, .T. ) ;
#5901=CARTESIAN_POINT ( 'NONE',  ( -12.50000000000000000, -24.99999999999999645, -3.235013004037443297E-15 ) ) ;
#5906=CARTESIAN_POINT ( 'NONE',  ( -12.50000000000000000, 1.530808498934191521E-15, 12.50000000000000000 ) ) ;
#5916=DIRECTION ( 'NONE',  ( 0.000000000000000000, 0.000000000000000000, -1.000000000000000000 ) ) ;
#5918=ORIENTED_EDGE ( 'NONE', *, *, #5520, .T. ) ;
#5925=DIRECTION ( 'NONE',  ( -0.000000000000000000, 0.000000000000000000, 1.000000000000000000 ) ) ;
#5931=ORIENTED_EDGE ( 'NONE', *, *, #6185, .T. ) ;
#5941=LINE ( 'NONE', #4853, #5080 ) ;
#5945=AXIS2_PLACEMENT_3D ( 'NONE', #4347, #2434, #4868 ) ;
#5981=ORIENTED_EDGE ( 'NONE', *, *, #7522, .F. ) ;
#5998=EDGE_LOOP ( 'NONE', ( #5435, #823, #7038, #6841 ) ) ;
#6010=ADVANCED_FACE ( 'NONE', ( #656 ), #7398, .F. ) ;
#6018=AXIS2_PLACEMENT_3D ( 'NONE', #7193, #7269, #4129 ) ;
#6019=EDGE_LOOP ( 'NONE', ( #4041, #1463, #247, #5622, #6939 ) ) ;
#6055=EDGE_LOOP ( 'NONE', ( #1460, #2171 ) ) ;
#6076=EDGE_CURVE ( 'NONE', #3451, #646, #2778, .T. ) ;
#6083=DIRECTION ( 'NONE',  ( 1.000000000000000000, 0.000000000000000000, 0.000000000000000000 ) ) ;
#6084=LINE ( 'NONE', #1106, #4776 ) ;
#6119=ORIENTED_EDGE ( 'NONE', *, *, #3220, .F. ) ;
#6151=EDGE_CURVE ( 'NONE', #3922, #4349, #1566, .T. ) ;
#6157=ORIENTED_EDGE ( 'NONE', *, *, #2675, .F. ) ;
#6185=EDGE_CURVE ( 'NONE', #1064, #1390, #6267, .T. ) ;
#6218=ORIENTED_EDGE ( 'NONE', *, *, #1863, .F. ) ;
#6223=DIRECTION ( 'NONE',  ( 1.000000000000000000, 0.000000000000000000, -0.000000000000000000 ) ) ;
#6232=LINE ( 'NONE', #5712, #4649 ) ;
#6244=AXIS2_PLACEMENT_3D ( 'NONE', #959, #3040, #4003 ) ;
#6254=VERTEX_POINT ( 'NONE', #7752 ) ;
#6267=CIRCLE ( 'NONE', #6018, 12.50000000000000000 ) ;
#6273=VERTEX_POINT ( 'NONE', #3539 ) ;
#6281=CARTESIAN_POINT ( 'NONE',  ( 12.50000000000000000, 25.00000000000000355, 3.703880899869785475E-15 ) ) ;
#6289=DIRECTION ( 'NONE',  ( 1.000000000000000000, 0.000000000000000000, 0.000000000000000000 ) ) ;
#6291=ORIENTED_EDGE ( 'NONE', *, *, #717, .F. ) ;
#6295=ORIENTED_EDGE ( 'NONE', *, *, #2926, .T. ) ;
#6353=LINE ( 'NONE', #3309, #2543 ) ;
#6376=DIRECTION ( 'NONE',  ( 1.000000000000000000, 0.000000000000000000, 0.000000000000000000 ) ) ;
#6398=EDGE_CURVE ( 'NONE', #4349, #5068, #3715, .T. ) ;
#6408=ORIENTED_EDGE ( 'NONE', *, *, #1802, .T. ) ;
#6415=DIRECTION ( 'NONE',  ( 0.000000000000000000, 0.000000000000000000, -1.000000000000000000 ) ) ;
#6437=ORIENTED_EDGE ( 'NONE', *, *, #2526, .F. ) ;
#6466=CARTESIAN_POINT ( 'NONE',  ( -25.00000000000000000, 0.000000000000000000, 0.000000000000000000 ) ) ;
#6471=FACE_OUTER_BOUND ( 'NONE', #401, .T. ) ;
#6482=AXIS2_PLACEMENT_3D ( 'NONE', #7817, #4760, #6415 ) ;
#6483=VERTEX_POINT ( 'NONE', #3139 ) ;
#6489=VECTOR ( 'NONE', #3831, 1000.000000000000000 ) ;
#6512=FACE_OUTER_BOUND ( 'NONE', #6928, .T. ) ;
#6513=CARTESIAN_POINT ( 'NONE',  ( -25.00000000000000000, 25.00000000000000000, 0.000000000000000000 ) ) ;
#6514=AXIS2_PLACEMENT_3D ( 'NONE', #3930, #6376, #5087 ) ;
#6520=AXIS2_PLACEMENT_3D ( 'NONE', #7728, #4077, #4672 ) ;
#6559=CARTESIAN_POINT ( 'NONE',  ( -25.00000000000000000, 24.99999999999999289, 50.00000000000000000 ) ) ;
#6570=EDGE_CURVE ( 'NONE', #107, #3922, #1763, .T. ) ;
#6600=CIRCLE ( 'NONE', #191, 25.00000000000000000 ) ;
#6602=ORIENTED_EDGE ( 'NONE', *, *, #5885, .T. ) ;
#6603=VECTOR ( 'NONE', #3343, 1000.000000000000114 ) ;
#6623=EDGE_CURVE ( 'NONE', #6254, #7564, #5868, .T. ) ;
#6638=VERTEX_POINT ( 'NONE', #4048 ) ;
#6648=VECTOR ( 'NONE', #4519, 1000.000000000000000 ) ;
#6655=ORIENTED_EDGE ( 'NONE', *, *, #7339, .F. ) ;
#6668=DIRECTION ( 'NONE',  ( -1.000000000000000000, -0.000000000000000000, -0.000000000000000000 ) ) ;
#6673=FACE_OUTER_BOUND ( 'NONE', #6019, .T. ) ;
#6678=ORIENTED_EDGE ( 'NONE', *, *, #2340, .F. ) ;
#6680=FACE_OUTER_BOUND ( 'NONE', #3243, .T. ) ;
#6684=VERTEX_POINT ( 'NONE', #7740 ) ;
#6687=EDGE_LOOP ( 'NONE', ( #7490, #2713, #5981, #1084, #5291, #3943, #550, #6119 ) ) ;
#6700=DIRECTION ( 'NONE',  ( 0.000000000000000000, 0.000000000000000000, -1.000000000000000000 ) ) ;
#6713=VECTOR ( 'NONE', #3107, 1000.000000000000000 ) ;
#6730=ORIENTED_EDGE ( 'NONE', *, *, #4738, .F. ) ;
#6745=CIRCLE ( 'NONE', #976, 11.64999999999996660 ) ;
#6754=DIRECTION ( 'NONE',  ( 1.000000000000000000, 0.000000000000000000, 0.000000000000000000 ) ) ;
#6806=LINE ( 'NONE', #3160, #6603 ) ;
#6840=CARTESIAN_POINT ( 'NONE',  ( -25.00000000000000000, 0.000000000000000000, 0.000000000000000000 ) ) ;
#6841=ORIENTED_EDGE ( 'NONE', *, *, #6858, .T. ) ;
#6847=ORIENTED_EDGE ( 'NONE', *, *, #5885, .F. ) ;
#6858=EDGE_CURVE ( 'NONE', #4661, #6638, #5148, .T. ) ;
#6886=UNCERTAINTY_MEASURE_WITH_UNIT (LENGTH_MEASURE( 1.000000000000000082E-05 ), #1146, 'distance_accuracy_value', 'NONE');
#6893=DIRECTION ( 'NONE',  ( -0.000000000000000000, -0.000000000000000000, -1.000000000000000000 ) ) ;
#6913=DIRECTION ( 'NONE',  ( 0.000000000000000000, -1.387778780781445676E-16, 1.000000000000000000 ) ) ;
#6928=EDGE_LOOP ( 'NONE', ( #5336, #2475, #1159, #5028 ) ) ;
#6934=PRODUCT_DEFINITION_FORMATION_WITH_SPECIFIED_SOURCE ( 'ANY', '', #3858, .NOT_KNOWN. ) ;
#6935=EDGE_LOOP ( 'NONE', ( #2404, #4363, #874, #2437 ) ) ;
#6936=LINE ( 'NONE', #995, #6648 ) ;
#6938=EDGE_CURVE ( 'NONE', #2333, #6684, #872, .T. ) ;
#6939=ORIENTED_EDGE ( 'NONE', *, *, #1528, .T. ) ;
#6961=UNCERTAINTY_MEASURE_WITH_UNIT (LENGTH_MEASURE( 1.000000000000000082E-05 ), #4632, 'distance_accuracy_value', 'NONE');
#6963=ORIENTED_EDGE ( 'NONE', *, *, #1080, .T. ) ;
#6964=ADVANCED_FACE ( 'NONE', ( #831, #2071 ), #6969, .F. ) ;
#6969=PLANE ( 'NONE',  #3823 ) ;
#6976=ORIENTED_EDGE ( 'NONE', *, *, #5419, .T. ) ;
#6980=VECTOR ( 'NONE', #3871, 1000.000000000000000 ) ;
#6982=FACE_OUTER_BOUND ( 'NONE', #4323, .T. ) ;
#7007=CARTESIAN_POINT ( 'NONE',  ( -25.00000000000000000, 0.000000000000000000, -25.00000000000000000 ) ) ;
#7010=MANIFOLD_SOLID_BREP ( 'Pah1', #2090 ) ;
#7013=ADVANCED_FACE ( 'NONE', ( #2846 ), #947, .T. ) ;
#7038=ORIENTED_EDGE ( 'NONE', *, *, #2187, .F. ) ;
#7041=FACE_OUTER_BOUND ( 'NONE', #2620, .T. ) ;
#7042=FACE_OUTER_BOUND ( 'NONE', #2589, .T. ) ;
#7054=DIRECTION ( 'NONE',  ( 1.000000000000000000, 0.000000000000000000, 0.000000000000000000 ) ) ;
#7056=CYLINDRICAL_SURFACE ( 'NONE', #3033, 25.00000000000000000 ) ;
#7067=CARTESIAN_POINT ( 'NONE',  ( -12.50000000000000000, -25.00000000000000355, 37.50000000000000000 ) ) ;
#7075=CARTESIAN_POINT ( 'NONE',  ( -25.00000000000000000, 25.00000000000000000, 0.000000000000000000 ) ) ;
#7119=DIRECTION ( 'NONE',  ( 1.000000000000000000, 0.000000000000000000, 0.000000000000000000 ) ) ;
#7138=ORIENTED_EDGE ( 'NONE', *, *, #6623, .T. ) ;
#7144=AXIS2_PLACEMENT_3D ( 'NONE', #7751, #2372, #6700 ) ;
#7170=ORIENTED_EDGE ( 'NONE', *, *, #1504, .T. ) ;
#7173=( NAMED_UNIT ( * ) PLANE_ANGLE_UNIT ( ) SI_UNIT ( $, .RADIAN. ) );
#7185=EDGE_LOOP ( 'NONE', ( #2630, #408, #2107, #3346 ) ) ;
#7192=CARTESIAN_POINT ( 'NONE',  ( -12.50000000000000000, -24.99999999999999645, -3.235013004037443297E-15 ) ) ;
#7193=CARTESIAN_POINT ( 'NONE',  ( 25.00000000000000000, 0.000000000000000000, 0.000000000000000000 ) ) ;
#7205=EDGE_LOOP ( 'NONE', ( #5379, #3546, #6295, #2958 ) ) ;
#7207=ADVANCED_FACE ( 'NONE', ( #6471 ), #1695, .T. ) ;
#7211=CARTESIAN_POINT ( 'NONE',  ( 0.000000000000000000, 0.000000000000000000, 200.0000000000000000 ) ) ;
#7228=DIRECTION ( 'NONE',  ( 0.000000000000000000, 0.000000000000000000, 1.000000000000000000 ) ) ;
#7238=DIRECTION ( 'NONE',  ( 0.000000000000000000, 0.000000000000000000, -1.000000000000000000 ) ) ;
#7269=DIRECTION ( 'NONE',  ( 1.000000000000000000, 0.000000000000000000, 0.000000000000000000 ) ) ;
#7272=CARTESIAN_POINT ( 'NONE',  ( 12.50000000000000355, 0.000000000000000000, 0.000000000000000000 ) ) ;
#7286=AXIS2_PLACEMENT_3D ( 'NONE', #4337, #5053, #7508 ) ;
#7289=CARTESIAN_POINT ( 'NONE',  ( -25.00000000000000000, 0.000000000000000000, 0.000000000000000000 ) ) ;
#7302=AXIS2_PLACEMENT_3D ( 'NONE', #526, #7783, #5857 ) ;
#7305=DIRECTION ( 'NONE',  ( 0.000000000000000000, -1.000000000000000000, 0.000000000000000000 ) ) ;
#7327=DIRECTION ( 'NONE',  ( 1.000000000000000000, 0.000000000000000000, 0.000000000000000000 ) ) ;
#7330=DIRECTION ( 'NONE',  ( -1.000000000000000000, 0.000000000000000000, 0.000000000000000000 ) ) ;
#7339=EDGE_CURVE ( 'NONE', #4682, #6684, #7867, .T. ) ;
#7347=CARTESIAN_POINT ( 'NONE',  ( -12.50000000000000000, 0.000000000000000000, 0.000000000000000000 ) ) ;
#7355=VECTOR ( 'NONE', #7327, 1000.000000000000000 ) ;
#7361=AXIS2_PLACEMENT_3D ( 'NONE', #5901, #2857, #2771 ) ;
#7374=EDGE_LOOP ( 'NONE', ( #5676, #4227 ) ) ;
#7384=ORIENTED_EDGE ( 'NONE', *, *, #147, .F. ) ;
#7389=DIRECTION ( 'NONE',  ( 0.000000000000000000, 0.000000000000000000, 1.000000000000000000 ) ) ;
#7398=CYLINDRICAL_SURFACE ( 'NONE', #7286, 12.50000000000000000 ) ;
#7403=EDGE_LOOP ( 'NONE', ( #1670, #6437 ) ) ;
#7424=VECTOR ( 'NONE', #5130, 1000.000000000000000 ) ;
#7437=CARTESIAN_POINT ( 'NONE',  ( -25.00000000000000000, 24.99999999999999289, 50.00000000000000000 ) ) ;
#7443=ORIENTED_EDGE ( 'NONE', *, *, #5793, .F. ) ;
#7468=PRODUCT_DEFINITION ( 'UNKNOWN', '', #6934, #1668 ) ;
#7470=LINE ( 'NONE', #619, #5754 ) ;
#7488=FACE_OUTER_BOUND ( 'NONE', #1679, .T. ) ;
#7490=ORIENTED_EDGE ( 'NONE', *, *, #1528, .F. ) ;
#7505=ORIENTED_EDGE ( 'NONE', *, *, #6623, .F. ) ;
#7508=DIRECTION ( 'NONE',  ( 0.000000000000000000, 0.000000000000000000, -1.000000000000000000 ) ) ;
#7514=EDGE_CURVE ( 'NONE', #4039, #1064, #915, .T. ) ;
#7522=EDGE_CURVE ( 'NONE', #5068, #6638, #6936, .T. ) ;
#7534=CONICAL_SURFACE ( 'NONE', #4072, 11.64999999999996660, 0.7853981633974482790 ) ;
#7564=VERTEX_POINT ( 'NONE', #875 ) ;
#7575=EDGE_CURVE ( 'NONE', #107, #1830, #7613, .T. ) ;
#7588=DIRECTION ( 'NONE',  ( 0.000000000000000000, -1.000000000000000000, -1.387778780781445676E-16 ) ) ;
#7595=PLANE ( 'NONE',  #1329 ) ;
#7602=CARTESIAN_POINT ( 'NONE',  ( 25.00000000000000000, 25.00000000000000000, 0.000000000000000000 ) ) ;
#7613=LINE ( 'NONE', #5243, #4083 ) ;
#7620=VERTEX_POINT ( 'NONE', #1073 ) ;
#7633=DIRECTION ( 'NONE',  ( -0.000000000000000000, 1.000000000000000000, 1.387778780781445676E-16 ) ) ;
#7722=( NAMED_UNIT ( * ) SI_UNIT ( $, .STERADIAN. ) SOLID_ANGLE_UNIT ( ) );
#7728=CARTESIAN_POINT ( 'NONE',  ( 0.000000000000000000, 0.000000000000000000, 200.0000000000000000 ) ) ;
#7740=CARTESIAN_POINT ( 'NONE',  ( -15.64999999999999680, 0.000000000000000000, 195.9999999999999716 ) ) ;
#7751=CARTESIAN_POINT ( 'NONE',  ( 12.50000000000000355, 0.000000000000000000, 0.000000000000000000 ) ) ;
#7752=CARTESIAN_POINT ( 'NONE',  ( -25.00000000000000000, 1.530808498934191521E-15, 12.50000000000000000 ) ) ;
#7754=CYLINDRICAL_SURFACE ( 'NONE', #5297, 12.50000000000000000 ) ;
#7762=DIRECTION ( 'NONE',  ( -0.000000000000000000, 1.000000000000000000, 1.387778780781445676E-16 ) ) ;
#7775=ADVANCED_FACE ( 'NONE', ( #7488 ), #2169, .T. ) ;
#7783=DIRECTION ( 'NONE',  ( 1.000000000000000000, 0.000000000000000000, 0.000000000000000000 ) ) ;
#7811=FACE_BOUND ( 'NONE', #7403, .T. ) ;
#7817=CARTESIAN_POINT ( 'NONE',  ( -25.00000000000000000, 0.000000000000000000, 0.000000000000000000 ) ) ;
#7818=VERTEX_POINT ( 'NONE', #7602 ) ;
#7838=CARTESIAN_POINT ( 'NONE',  ( 15.64999999999999680, 1.916572240665607593E-15, 200.0000000000000000 ) ) ;
#7844=DIRECTION ( 'NONE',  ( 0.000000000000000000, -1.000000000000000000, 0.000000000000000000 ) ) ;
#7867=LINE ( 'NONE', #582, #5370 ) ;
#7942=COLOUR_RGB('Light Blue',0.38,0.62,0.78);
#7943=FILL_AREA_STYLE_COLOUR('',#7942);
#7944=FILL_AREA_STYLE('',(#7943));
#7945=SURFACE_STYLE_FILL_AREA(#7944);
#7946=SURFACE_SIDE_STYLE('',(#7945));
#7947=SURFACE_STYLE_USAGE(.BOTH.,#7946);
#7948=PRESENTATION_STYLE_ASSIGNMENT((#7947));
ENDSEC;
END-ISO-10303-21;
